ISO-10303-21;
HEADER;
/* Generated by software containing ST-Developer
 * from STEP Tools, Inc. (www.steptools.com) 
 */

FILE_DESCRIPTION(
/* description */ ('Bell-crank linkage with push rods'),
/* implementation_level */ '2;1');

FILE_NAME(
/* name */ 'Foot strip (1).step',
/* time_stamp */ '2026-10-28T03:25:15-07:00',
/* author */ (''),
/* organization */ (''),
/* preprocessor_version */ 'ST-DEVELOPER v20.2',
/* originating_system */ 'Autodesk Translation Framework v15.17.0.0',
/* authorisation */ '');

FILE_SCHEMA (('AUTOMOTIVE_DESIGN { 1 0 10303 214 3 1 1 }'));
ENDSEC;

DATA;
#10=MECHANICAL_DESIGN_GEOMETRIC_PRESENTATION_REPRESENTATION('',(#606),#16678);
#498=SHAPE_REPRESENTATION_RELATIONSHIP('SRR','None',#16914,#552);
#552=ADVANCED_BREP_SHAPE_REPRESENTATION('',(#668),#16619);
#606=STYLED_ITEM('',(#17277),#668);
#668=MANIFOLD_SOLID_BREP('Body1',#8796);
#978=PLANE('',#9507);
#979=PLANE('',#9508);
#980=PLANE('',#9509);
#981=PLANE('',#9510);
#982=PLANE('',#9511);
#983=PLANE('',#9512);
#1271=FACE_OUTER_BOUND('',#1817,.T.);
#1272=FACE_OUTER_BOUND('',#1818,.T.);
#1273=FACE_OUTER_BOUND('',#1819,.T.);
#1274=FACE_OUTER_BOUND('',#1820,.T.);
#1275=FACE_OUTER_BOUND('',#1821,.T.);
#1276=FACE_OUTER_BOUND('',#1822,.T.);
#1817=EDGE_LOOP('',(#6031,#6032,#6033,#6034));
#1818=EDGE_LOOP('',(#6035,#6036,#6037,#6038));
#1819=EDGE_LOOP('',(#6039,#6040,#6041,#6042));
#1820=EDGE_LOOP('',(#6043,#6044,#6045,#6046));
#1821=EDGE_LOOP('',(#6047,#6048,#6049,#6050));
#1822=EDGE_LOOP('',(#6051,#6052,#6053,#6054));
#2568=LINE('',#13663,#3117);
#2569=LINE('',#13665,#3118);
#2570=LINE('',#13667,#3119);
#2571=LINE('',#13668,#3120);
#2572=LINE('',#13671,#3121);
#2573=LINE('',#13673,#3122);
#2574=LINE('',#13674,#3123);
#2575=LINE('',#13677,#3124);
#2576=LINE('',#13679,#3125);
#2577=LINE('',#13680,#3126);
#2578=LINE('',#13682,#3127);
#2579=LINE('',#13683,#3128);
#3117=VECTOR('',#10774,1.);
#3118=VECTOR('',#10775,1.);
#3119=VECTOR('',#10776,1.);
#3120=VECTOR('',#10777,1.);
#3121=VECTOR('',#10780,1.);
#3122=VECTOR('',#10781,1.);
#3123=VECTOR('',#10782,1.);
#3124=VECTOR('',#10785,1.);
#3125=VECTOR('',#10786,1.);
#3126=VECTOR('',#10787,1.);
#3127=VECTOR('',#10790,1.);
#3128=VECTOR('',#10791,1.);
#4160=VERTEX_POINT('',#13661);
#4161=VERTEX_POINT('',#13662);
#4162=VERTEX_POINT('',#13664);
#4163=VERTEX_POINT('',#13666);
#4164=VERTEX_POINT('',#13670);
#4165=VERTEX_POINT('',#13672);
#4166=VERTEX_POINT('',#13676);
#4167=VERTEX_POINT('',#13678);
#4893=EDGE_CURVE('',#4160,#4161,#2568,.T.);
#4894=EDGE_CURVE('',#4161,#4162,#2569,.T.);
#4895=EDGE_CURVE('',#4163,#4162,#2570,.T.);
#4896=EDGE_CURVE('',#4160,#4163,#2571,.T.);
#4897=EDGE_CURVE('',#4164,#4160,#2572,.T.);
#4898=EDGE_CURVE('',#4165,#4163,#2573,.T.);
#4899=EDGE_CURVE('',#4164,#4165,#2574,.T.);
#4900=EDGE_CURVE('',#4166,#4164,#2575,.T.);
#4901=EDGE_CURVE('',#4167,#4165,#2576,.T.);
#4902=EDGE_CURVE('',#4166,#4167,#2577,.T.);
#4903=EDGE_CURVE('',#4161,#4166,#2578,.T.);
#4904=EDGE_CURVE('',#4162,#4167,#2579,.T.);
#6031=ORIENTED_EDGE('',*,*,#4893,.T.);
#6032=ORIENTED_EDGE('',*,*,#4894,.T.);
#6033=ORIENTED_EDGE('',*,*,#4895,.F.);
#6034=ORIENTED_EDGE('',*,*,#4896,.F.);
#6035=ORIENTED_EDGE('',*,*,#4897,.T.);
#6036=ORIENTED_EDGE('',*,*,#4896,.T.);
#6037=ORIENTED_EDGE('',*,*,#4898,.F.);
#6038=ORIENTED_EDGE('',*,*,#4899,.F.);
#6039=ORIENTED_EDGE('',*,*,#4900,.T.);
#6040=ORIENTED_EDGE('',*,*,#4899,.T.);
#6041=ORIENTED_EDGE('',*,*,#4901,.F.);
#6042=ORIENTED_EDGE('',*,*,#4902,.F.);
#6043=ORIENTED_EDGE('',*,*,#4903,.T.);
#6044=ORIENTED_EDGE('',*,*,#4902,.T.);
#6045=ORIENTED_EDGE('',*,*,#4904,.F.);
#6046=ORIENTED_EDGE('',*,*,#4894,.F.);
#6047=ORIENTED_EDGE('',*,*,#4904,.T.);
#6048=ORIENTED_EDGE('',*,*,#4901,.T.);
#6049=ORIENTED_EDGE('',*,*,#4898,.T.);
#6050=ORIENTED_EDGE('',*,*,#4895,.T.);
#6051=ORIENTED_EDGE('',*,*,#4903,.F.);
#6052=ORIENTED_EDGE('',*,*,#4893,.F.);
#6053=ORIENTED_EDGE('',*,*,#4897,.F.);
#6054=ORIENTED_EDGE('',*,*,#4900,.F.);
#8296=ADVANCED_FACE('',(#1271),#978,.T.);
#8297=ADVANCED_FACE('',(#1272),#979,.T.);
#8298=ADVANCED_FACE('',(#1273),#980,.T.);
#8299=ADVANCED_FACE('',(#1274),#981,.T.);
#8300=ADVANCED_FACE('',(#1275),#982,.T.);
#8301=ADVANCED_FACE('',(#1276),#983,.F.);
#8796=CLOSED_SHELL('',(#8296,#8297,#8298,#8299,#8300,#8301));
#9506=AXIS2_PLACEMENT_3D('',#13659,#10770,#10771);
#9507=AXIS2_PLACEMENT_3D('',#13660,#10772,#10773);
#9508=AXIS2_PLACEMENT_3D('',#13669,#10778,#10779);
#9509=AXIS2_PLACEMENT_3D('',#13675,#10783,#10784);
#9510=AXIS2_PLACEMENT_3D('',#13681,#10788,#10789);
#9511=AXIS2_PLACEMENT_3D('',#13684,#10792,#10793);
#9512=AXIS2_PLACEMENT_3D('',#13685,#10794,#10795);
#10770=DIRECTION('axis',(0.,0.,1.));
#10771=DIRECTION('refdir',(1.,0.,0.));
#10772=DIRECTION('center_axis',(0.,1.,0.));
#10773=DIRECTION('ref_axis',(-1.,0.,0.));
#10774=DIRECTION('',(-1.,0.,0.));
#10775=DIRECTION('',(0.,0.,1.));
#10776=DIRECTION('',(-1.,0.,0.));
#10777=DIRECTION('',(0.,0.,1.));
#10778=DIRECTION('center_axis',(1.,0.,0.));
#10779=DIRECTION('ref_axis',(0.,1.,0.));
#10780=DIRECTION('',(0.,1.,0.));
#10781=DIRECTION('',(0.,1.,0.));
#10782=DIRECTION('',(0.,0.,1.));
#10783=DIRECTION('center_axis',(0.,-1.,0.));
#10784=DIRECTION('ref_axis',(1.,0.,0.));
#10785=DIRECTION('',(1.,0.,0.));
#10786=DIRECTION('',(1.,0.,0.));
#10787=DIRECTION('',(0.,0.,1.));
#10788=DIRECTION('center_axis',(-1.,0.,0.));
#10789=DIRECTION('ref_axis',(0.,-1.,0.));
#10790=DIRECTION('',(0.,-1.,0.));
#10791=DIRECTION('',(0.,-1.,0.));
#10792=DIRECTION('center_axis',(0.,0.,1.));
#10793=DIRECTION('ref_axis',(1.,0.,0.));
#10794=DIRECTION('center_axis',(0.,0.,1.));
#10795=DIRECTION('ref_axis',(1.,0.,0.));
#13659=CARTESIAN_POINT('',(0.,0.,0.));
#13660=CARTESIAN_POINT('Origin',(17.,19.,-0.8));
#13661=CARTESIAN_POINT('',(17.,19.,-0.8));
#13662=CARTESIAN_POINT('',(16.,19.,-0.8));
#13663=CARTESIAN_POINT('',(17.,19.,-0.8));
#13664=CARTESIAN_POINT('',(16.,19.,0.));
#13665=CARTESIAN_POINT('',(16.,19.,-0.8));
#13666=CARTESIAN_POINT('',(17.,19.,0.));
#13667=CARTESIAN_POINT('',(17.,19.,0.));
#13668=CARTESIAN_POINT('',(17.,19.,-0.8));
#13669=CARTESIAN_POINT('Origin',(17.,-4.,-0.8));
#13670=CARTESIAN_POINT('',(17.,-4.,-0.8));
#13671=CARTESIAN_POINT('',(17.,-4.,-0.8));
#13672=CARTESIAN_POINT('',(17.,-4.,0.));
#13673=CARTESIAN_POINT('',(17.,-4.,0.));
#13674=CARTESIAN_POINT('',(17.,-4.,-0.8));
#13675=CARTESIAN_POINT('Origin',(16.,-4.,-0.8));
#13676=CARTESIAN_POINT('',(16.,-4.,-0.8));
#13677=CARTESIAN_POINT('',(16.,-4.,-0.8));
#13678=CARTESIAN_POINT('',(16.,-4.,0.));
#13679=CARTESIAN_POINT('',(16.,-4.,0.));
#13680=CARTESIAN_POINT('',(16.,-4.,-0.8));
#13681=CARTESIAN_POINT('Origin',(16.,19.,-0.8));
#13682=CARTESIAN_POINT('',(16.,19.,-0.8));
#13683=CARTESIAN_POINT('',(16.,19.,0.));
#13684=CARTESIAN_POINT('Origin',(16.5,7.5,0.));
#13685=CARTESIAN_POINT('Origin',(16.5,7.5,-0.8));
#16555=UNCERTAINTY_MEASURE_WITH_UNIT(LENGTH_MEASURE(0.001),#16679,
'DISTANCE_ACCURACY_VALUE',
'Maximum model space distance between geometric entities at asserted c
onnectivities');
#16614=UNCERTAINTY_MEASURE_WITH_UNIT(LENGTH_MEASURE(0.001),#16679,
'DISTANCE_ACCURACY_VALUE',
'Maximum model space distance between geometric entities at asserted c
onnectivities');
#16619=(
GEOMETRIC_REPRESENTATION_CONTEXT(3)
GLOBAL_UNCERTAINTY_ASSIGNED_CONTEXT((#16555))
GLOBAL_UNIT_ASSIGNED_CONTEXT((#16679,#16681,#16682))
REPRESENTATION_CONTEXT('','3D')
);
#16678=(
GEOMETRIC_REPRESENTATION_CONTEXT(3)
GLOBAL_UNCERTAINTY_ASSIGNED_CONTEXT((#16614))
GLOBAL_UNIT_ASSIGNED_CONTEXT((#16679,#16681,#16682))
REPRESENTATION_CONTEXT('','3D')
);
#16679=(
LENGTH_UNIT()
NAMED_UNIT(*)
SI_UNIT(.CENTI.,.METRE.)
);
#16681=(
NAMED_UNIT(*)
PLANE_ANGLE_UNIT()
SI_UNIT($,.RADIAN.)
);
#16682=(
NAMED_UNIT(*)
SI_UNIT($,.STERADIAN.)
SOLID_ANGLE_UNIT()
);
#16687=SHAPE_DEFINITION_REPRESENTATION(#16750,#16914);
#16750=PRODUCT_DEFINITION_SHAPE('',$,#16978);
#16914=SHAPE_REPRESENTATION('',(#9506),#16619);
#16973=PRODUCT_DEFINITION_CONTEXT('part definition',#17164,'design');
#16978=PRODUCT_DEFINITION('Foot strip (1)','Foot strip (1)',#17041,#16973);
#17041=PRODUCT_DEFINITION_FORMATION('',$,#17170);
#17164=APPLICATION_CONTEXT(
'Core Data for Automotive Mechanical Design Process');
#17165=PRODUCT_CONTEXT('part definition',#17164,'mechanical');
#17170=PRODUCT('Foot strip (1)','Foot strip (1)','Foot strip (1)',(#17165));
#17271=COLOUR_RGB('Light Blue',0.38,0.62,0.78);
#17272=FILL_AREA_STYLE_COLOUR('',#17271);
#17273=FILL_AREA_STYLE('',(#17272));
#17274=SURFACE_STYLE_FILL_AREA(#17273);
#17275=SURFACE_SIDE_STYLE('',(#17274));
#17276=SURFACE_STYLE_USAGE(.BOTH.,#17275);
#17277=PRESENTATION_STYLE_ASSIGNMENT((#17276));
ENDSEC;
END-ISO-10303-21;
